ISO-10303-21;
HEADER;
/* Generated by software containing ST-Developer
 * from STEP Tools, Inc. (www.steptools.com) 
 */

FILE_DESCRIPTION(
/* description */ ('Four-bar parallelogram arm'),
/* implementation_level */ '2;1');

FILE_NAME(
/* name */ 'Rear inner spacer (1).step',
/* time_stamp */ '2026-10-28T03:24:55-07:00',
/* author */ (''),
/* organization */ (''),
/* preprocessor_version */ 'ST-DEVELOPER v20.2',
/* originating_system */ 'Autodesk Translation Framework v15.17.0.0',
/* authorisation */ '');

FILE_SCHEMA (('AUTOMOTIVE_DESIGN { 1 0 10303 214 3 1 1 }'));
ENDSEC;

DATA;
#10=MECHANICAL_DESIGN_GEOMETRIC_PRESENTATION_REPRESENTATION('',(#633),#14512);
#533=SHAPE_REPRESENTATION_RELATIONSHIP('SRR','None',#14754,#583);
#583=ADVANCED_BREP_SHAPE_REPRESENTATION('',(#691),#14469);
#633=STYLED_ITEM('',(#15080),#691);
#691=MANIFOLD_SOLID_BREP('Body1',#7337);
#796=FACE_BOUND('',#1775,.T.);
#797=FACE_BOUND('',#1777,.T.);
#1055=PLANE('',#8130);
#1056=PLANE('',#8131);
#1291=FACE_OUTER_BOUND('',#1772,.T.);
#1292=FACE_OUTER_BOUND('',#1773,.T.);
#1293=FACE_OUTER_BOUND('',#1774,.T.);
#1294=FACE_OUTER_BOUND('',#1776,.T.);
#1772=EDGE_LOOP('',(#5354,#5355,#5356,#5357));
#1773=EDGE_LOOP('',(#5358,#5359,#5360,#5361));
#1774=EDGE_LOOP('',(#5362));
#1775=EDGE_LOOP('',(#5363));
#1776=EDGE_LOOP('',(#5364));
#1777=EDGE_LOOP('',(#5365));
#2413=LINE('',#11841,#2807);
#2414=LINE('',#11847,#2808);
#2807=VECTOR('',#9447,0.505);
#2808=VECTOR('',#9454,0.7);
#3182=CIRCLE('',#8125,0.505);
#3183=CIRCLE('',#8126,0.505);
#3184=CIRCLE('',#8128,0.7);
#3185=CIRCLE('',#8129,0.7);
#3667=VERTEX_POINT('',#11838);
#3668=VERTEX_POINT('',#11840);
#3669=VERTEX_POINT('',#11844);
#3670=VERTEX_POINT('',#11846);
#4308=EDGE_CURVE('',#3667,#3667,#3182,.T.);
#4309=EDGE_CURVE('',#3667,#3668,#2413,.T.);
#4310=EDGE_CURVE('',#3668,#3668,#3183,.T.);
#4311=EDGE_CURVE('',#3669,#3669,#3184,.T.);
#4312=EDGE_CURVE('',#3669,#3670,#2414,.T.);
#4313=EDGE_CURVE('',#3670,#3670,#3185,.T.);
#5354=ORIENTED_EDGE('',*,*,#4308,.F.);
#5355=ORIENTED_EDGE('',*,*,#4309,.T.);
#5356=ORIENTED_EDGE('',*,*,#4310,.T.);
#5357=ORIENTED_EDGE('',*,*,#4309,.F.);
#5358=ORIENTED_EDGE('',*,*,#4311,.F.);
#5359=ORIENTED_EDGE('',*,*,#4312,.T.);
#5360=ORIENTED_EDGE('',*,*,#4313,.T.);
#5361=ORIENTED_EDGE('',*,*,#4312,.F.);
#5362=ORIENTED_EDGE('',*,*,#4311,.T.);
#5363=ORIENTED_EDGE('',*,*,#4308,.T.);
#5364=ORIENTED_EDGE('',*,*,#4313,.F.);
#5365=ORIENTED_EDGE('',*,*,#4310,.F.);
#6755=CYLINDRICAL_SURFACE('',#8124,0.505);
#6756=CYLINDRICAL_SURFACE('',#8127,0.7);
#6996=ADVANCED_FACE('',(#1291),#6755,.F.);
#6997=ADVANCED_FACE('',(#1292),#6756,.T.);
#6998=ADVANCED_FACE('',(#1293,#796),#1055,.T.);
#6999=ADVANCED_FACE('',(#1294,#797),#1056,.F.);
#7337=CLOSED_SHELL('',(#6996,#6997,#6998,#6999));
#8123=AXIS2_PLACEMENT_3D('',#11836,#9441,#9442);
#8124=AXIS2_PLACEMENT_3D('',#11837,#9443,#9444);
#8125=AXIS2_PLACEMENT_3D('',#11839,#9445,#9446);
#8126=AXIS2_PLACEMENT_3D('',#11842,#9448,#9449);
#8127=AXIS2_PLACEMENT_3D('',#11843,#9450,#9451);
#8128=AXIS2_PLACEMENT_3D('',#11845,#9452,#9453);
#8129=AXIS2_PLACEMENT_3D('',#11848,#9455,#9456);
#8130=AXIS2_PLACEMENT_3D('',#11849,#9457,#9458);
#8131=AXIS2_PLACEMENT_3D('',#11850,#9459,#9460);
#9441=DIRECTION('axis',(0.,0.,1.));
#9442=DIRECTION('refdir',(1.,0.,0.));
#9443=DIRECTION('center_axis',(0.,1.,0.));
#9444=DIRECTION('ref_axis',(1.,0.,0.));
#9445=DIRECTION('center_axis',(0.,-1.,0.));
#9446=DIRECTION('ref_axis',(1.,0.,0.));
#9447=DIRECTION('',(0.,-1.,0.));
#9448=DIRECTION('center_axis',(0.,-1.,0.));
#9449=DIRECTION('ref_axis',(1.,0.,0.));
#9450=DIRECTION('center_axis',(0.,1.,0.));
#9451=DIRECTION('ref_axis',(1.,0.,0.));
#9452=DIRECTION('center_axis',(0.,1.,0.));
#9453=DIRECTION('ref_axis',(1.,0.,0.));
#9454=DIRECTION('',(0.,-1.,0.));
#9455=DIRECTION('center_axis',(0.,1.,0.));
#9456=DIRECTION('ref_axis',(1.,0.,0.));
#9457=DIRECTION('center_axis',(0.,1.,0.));
#9458=DIRECTION('ref_axis',(1.,0.,0.));
#9459=DIRECTION('center_axis',(0.,1.,0.));
#9460=DIRECTION('ref_axis',(1.,0.,0.));
#11836=CARTESIAN_POINT('',(0.,0.,0.));
#11837=CARTESIAN_POINT('Origin',(0.,1.05,14.));
#11838=CARTESIAN_POINT('',(-0.505,2.5,14.));
#11839=CARTESIAN_POINT('Origin',(0.,2.5,14.));
#11840=CARTESIAN_POINT('',(-0.505,1.05,14.));
#11841=CARTESIAN_POINT('',(-0.505,1.05,14.));
#11842=CARTESIAN_POINT('Origin',(0.,1.05,14.));
#11843=CARTESIAN_POINT('Origin',(0.,1.05,14.));
#11844=CARTESIAN_POINT('',(-0.7,2.5,14.));
#11845=CARTESIAN_POINT('Origin',(0.,2.5,14.));
#11846=CARTESIAN_POINT('',(-0.7,1.05,14.));
#11847=CARTESIAN_POINT('',(-0.7,1.05,14.));
#11848=CARTESIAN_POINT('Origin',(0.,1.05,14.));
#11849=CARTESIAN_POINT('Origin',(0.,2.5,14.));
#11850=CARTESIAN_POINT('Origin',(0.,1.05,14.));
#14412=UNCERTAINTY_MEASURE_WITH_UNIT(LENGTH_MEASURE(0.001),#14513,
'DISTANCE_ACCURACY_VALUE',
'Maximum model space distance between geometric entities at asserted c
onnectivities');
#14455=UNCERTAINTY_MEASURE_WITH_UNIT(LENGTH_MEASURE(0.001),#14513,
'DISTANCE_ACCURACY_VALUE',
'Maximum model space distance between geometric entities at asserted c
onnectivities');
#14469=(
GEOMETRIC_REPRESENTATION_CONTEXT(3)
GLOBAL_UNCERTAINTY_ASSIGNED_CONTEXT((#14412))
GLOBAL_UNIT_ASSIGNED_CONTEXT((#14513,#14515,#14516))
REPRESENTATION_CONTEXT('','3D')
);
#14512=(
GEOMETRIC_REPRESENTATION_CONTEXT(3)
GLOBAL_UNCERTAINTY_ASSIGNED_CONTEXT((#14455))
GLOBAL_UNIT_ASSIGNED_CONTEXT((#14513,#14515,#14516))
REPRESENTATION_CONTEXT('','3D')
);
#14513=(
LENGTH_UNIT()
NAMED_UNIT(*)
SI_UNIT(.CENTI.,.METRE.)
);
#14515=(
NAMED_UNIT(*)
PLANE_ANGLE_UNIT()
SI_UNIT($,.RADIAN.)
);
#14516=(
NAMED_UNIT(*)
SI_UNIT($,.STERADIAN.)
SOLID_ANGLE_UNIT()
);
#14530=SHAPE_DEFINITION_REPRESENTATION(#14586,#14754);
#14586=PRODUCT_DEFINITION_SHAPE('',$,#14811);
#14754=SHAPE_REPRESENTATION('',(#8123),#14469);
#14797=PRODUCT_DEFINITION_CONTEXT('part definition',#14967,'design');
#14811=PRODUCT_DEFINITION('Rear inner spacer (1)','Rear inner spacer (1)',
#14867,#14797);
#14867=PRODUCT_DEFINITION_FORMATION('',$,#14982);
#14967=APPLICATION_CONTEXT(
'Core Data for Automotive Mechanical Design Process');
#14968=PRODUCT_CONTEXT('part definition',#14967,'mechanical');
#14982=PRODUCT('Rear inner spacer (1)','Rear inner spacer (1)',
'Rear inner spacer (1)',(#14968));
#15074=COLOUR_RGB('Sky Blue',0.24,0.69,0.87);
#15075=FILL_AREA_STYLE_COLOUR('',#15074);
#15076=FILL_AREA_STYLE('',(#15075));
#15077=SURFACE_STYLE_FILL_AREA(#15076);
#15078=SURFACE_SIDE_STYLE('',(#15077));
#15079=SURFACE_STYLE_USAGE(.BOTH.,#15078);
#15080=PRESENTATION_STYLE_ASSIGNMENT((#15079));
ENDSEC;
END-ISO-10303-21;
